ISO-10303-21;
HEADER;
/* Generated by software containing ST-Developer
 * from STEP Tools, Inc. (www.steptools.com) 
 */

FILE_DESCRIPTION(
/* description */ ('PAT-091'),
/* implementation_level */ '2;1');

FILE_NAME(
/* name */ 'Plain pivot bush (9).step',
/* time_stamp */ '2026-10-27T15:34:44-07:00',
/* author */ (''),
/* organization */ (''),
/* preprocessor_version */ 'ST-DEVELOPER v20.2',
/* originating_system */ 'Autodesk Translation Framework v15.17.0.0',
/* authorisation */ '');

FILE_SCHEMA (('AUTOMOTIVE_DESIGN { 1 0 10303 214 3 1 1 }'));
ENDSEC;

DATA;
#10=MECHANICAL_DESIGN_GEOMETRIC_PRESENTATION_REPRESENTATION('',(#1059),#25100);
#839=SHAPE_REPRESENTATION_RELATIONSHIP('SRR','None',#25606,#949);
#949=ADVANCED_BREP_SHAPE_REPRESENTATION('',(#1180),#25076);
#1059=STYLED_ITEM('',(#26177),#1180);
#1180=MANIFOLD_SOLID_BREP('Body1',#13339);
#1587=FACE_BOUND('',#3908,.T.);
#1588=FACE_BOUND('',#3910,.T.);
#1994=PLANE('',#16008);
#1995=PLANE('',#16009);
#2715=FACE_OUTER_BOUND('',#3905,.T.);
#2716=FACE_OUTER_BOUND('',#3906,.T.);
#2717=FACE_OUTER_BOUND('',#3907,.T.);
#2718=FACE_OUTER_BOUND('',#3909,.T.);
#3905=EDGE_LOOP('',(#11528,#11529,#11530,#11531));
#3906=EDGE_LOOP('',(#11532,#11533,#11534,#11535));
#3907=EDGE_LOOP('',(#11536));
#3908=EDGE_LOOP('',(#11537));
#3909=EDGE_LOOP('',(#11538));
#3910=EDGE_LOOP('',(#11539));
#4804=LINE('',#23979,#5544);
#4805=LINE('',#23985,#5545);
#5544=VECTOR('',#19986,0.605);
#5545=VECTOR('',#19993,1.);
#6198=CIRCLE('',#16003,0.605);
#6199=CIRCLE('',#16004,0.605);
#6200=CIRCLE('',#16006,1.);
#6201=CIRCLE('',#16007,1.);
#7231=VERTEX_POINT('',#23976);
#7232=VERTEX_POINT('',#23978);
#7233=VERTEX_POINT('',#23982);
#7234=VERTEX_POINT('',#23984);
#8699=EDGE_CURVE('',#7231,#7231,#6198,.T.);
#8700=EDGE_CURVE('',#7231,#7232,#4804,.T.);
#8701=EDGE_CURVE('',#7232,#7232,#6199,.T.);
#8702=EDGE_CURVE('',#7233,#7233,#6200,.T.);
#8703=EDGE_CURVE('',#7233,#7234,#4805,.T.);
#8704=EDGE_CURVE('',#7234,#7234,#6201,.T.);
#11528=ORIENTED_EDGE('',*,*,#8699,.F.);
#11529=ORIENTED_EDGE('',*,*,#8700,.T.);
#11530=ORIENTED_EDGE('',*,*,#8701,.T.);
#11531=ORIENTED_EDGE('',*,*,#8700,.F.);
#11532=ORIENTED_EDGE('',*,*,#8702,.F.);
#11533=ORIENTED_EDGE('',*,*,#8703,.T.);
#11534=ORIENTED_EDGE('',*,*,#8704,.T.);
#11535=ORIENTED_EDGE('',*,*,#8703,.F.);
#11536=ORIENTED_EDGE('',*,*,#8702,.T.);
#11537=ORIENTED_EDGE('',*,*,#8699,.T.);
#11538=ORIENTED_EDGE('',*,*,#8704,.F.);
#11539=ORIENTED_EDGE('',*,*,#8701,.F.);
#12360=CYLINDRICAL_SURFACE('',#16002,0.605);
#12361=CYLINDRICAL_SURFACE('',#16005,1.);
#13082=ADVANCED_FACE('',(#2715),#12360,.F.);
#13083=ADVANCED_FACE('',(#2716),#12361,.T.);
#13084=ADVANCED_FACE('',(#2717,#1587),#1994,.T.);
#13085=ADVANCED_FACE('',(#2718,#1588),#1995,.F.);
#13339=CLOSED_SHELL('',(#13082,#13083,#13084,#13085));
#16001=AXIS2_PLACEMENT_3D('',#23974,#19980,#19981);
#16002=AXIS2_PLACEMENT_3D('',#23975,#19982,#19983);
#16003=AXIS2_PLACEMENT_3D('',#23977,#19984,#19985);
#16004=AXIS2_PLACEMENT_3D('',#23980,#19987,#19988);
#16005=AXIS2_PLACEMENT_3D('',#23981,#19989,#19990);
#16006=AXIS2_PLACEMENT_3D('',#23983,#19991,#19992);
#16007=AXIS2_PLACEMENT_3D('',#23986,#19994,#19995);
#16008=AXIS2_PLACEMENT_3D('',#23987,#19996,#19997);
#16009=AXIS2_PLACEMENT_3D('',#23988,#19998,#19999);
#19980=DIRECTION('axis',(0.,0.,1.));
#19981=DIRECTION('refdir',(1.,0.,0.));
#19982=DIRECTION('center_axis',(0.,1.,0.));
#19983=DIRECTION('ref_axis',(1.,0.,0.));
#19984=DIRECTION('center_axis',(0.,-1.,0.));
#19985=DIRECTION('ref_axis',(1.,0.,0.));
#19986=DIRECTION('',(0.,-1.,0.));
#19987=DIRECTION('center_axis',(0.,-1.,0.));
#19988=DIRECTION('ref_axis',(1.,0.,0.));
#19989=DIRECTION('center_axis',(0.,1.,0.));
#19990=DIRECTION('ref_axis',(1.,0.,0.));
#19991=DIRECTION('center_axis',(0.,1.,0.));
#19992=DIRECTION('ref_axis',(1.,0.,0.));
#19993=DIRECTION('',(0.,-1.,0.));
#19994=DIRECTION('center_axis',(0.,1.,0.));
#19995=DIRECTION('ref_axis',(1.,0.,0.));
#19996=DIRECTION('center_axis',(0.,1.,0.));
#19997=DIRECTION('ref_axis',(1.,0.,0.));
#19998=DIRECTION('center_axis',(0.,1.,0.));
#19999=DIRECTION('ref_axis',(1.,0.,0.));
#23974=CARTESIAN_POINT('',(0.,0.,0.));
#23975=CARTESIAN_POINT('Origin',(0.,7.,13.));
#23976=CARTESIAN_POINT('',(-0.605,8.,13.));
#23977=CARTESIAN_POINT('Origin',(0.,8.,13.));
#23978=CARTESIAN_POINT('',(-0.605,7.,13.));
#23979=CARTESIAN_POINT('',(-0.605,7.,13.));
#23980=CARTESIAN_POINT('Origin',(0.,7.,13.));
#23981=CARTESIAN_POINT('Origin',(0.,7.,13.));
#23982=CARTESIAN_POINT('',(-1.,8.,13.));
#23983=CARTESIAN_POINT('Origin',(0.,8.,13.));
#23984=CARTESIAN_POINT('',(-1.,7.,13.));
#23985=CARTESIAN_POINT('',(-1.,7.,13.));
#23986=CARTESIAN_POINT('Origin',(0.,7.,13.));
#23987=CARTESIAN_POINT('Origin',(0.,8.,13.));
#23988=CARTESIAN_POINT('Origin',(0.,7.,13.));
#24955=UNCERTAINTY_MEASURE_WITH_UNIT(LENGTH_MEASURE(0.001),#25101,
'DISTANCE_ACCURACY_VALUE',
'Maximum model space distance between geometric entities at asserted c
onnectivities');
#24979=UNCERTAINTY_MEASURE_WITH_UNIT(LENGTH_MEASURE(0.001),#25101,
'DISTANCE_ACCURACY_VALUE',
'Maximum model space distance between geometric entities at asserted c
onnectivities');
#25076=(
GEOMETRIC_REPRESENTATION_CONTEXT(3)
GLOBAL_UNCERTAINTY_ASSIGNED_CONTEXT((#24955))
GLOBAL_UNIT_ASSIGNED_CONTEXT((#25101,#25103,#25104))
REPRESENTATION_CONTEXT('','3D')
);
#25100=(
GEOMETRIC_REPRESENTATION_CONTEXT(3)
GLOBAL_UNCERTAINTY_ASSIGNED_CONTEXT((#24979))
GLOBAL_UNIT_ASSIGNED_CONTEXT((#25101,#25103,#25104))
REPRESENTATION_CONTEXT('','3D')
);
#25101=(
LENGTH_UNIT()
NAMED_UNIT(*)
SI_UNIT(.CENTI.,.METRE.)
);
#25103=(
NAMED_UNIT(*)
PLANE_ANGLE_UNIT()
SI_UNIT($,.RADIAN.)
);
#25104=(
NAMED_UNIT(*)
SI_UNIT($,.STERADIAN.)
SOLID_ANGLE_UNIT()
);
#25201=SHAPE_DEFINITION_REPRESENTATION(#25395,#25606);
#25395=PRODUCT_DEFINITION_SHAPE('',$,#25727);
#25606=SHAPE_REPRESENTATION('',(#16001),#25076);
#25630=PRODUCT_DEFINITION_CONTEXT('part definition',#25992,'design');
#25727=PRODUCT_DEFINITION('Plain pivot bush (9)','Plain pivot bush (9)',#25847,
#25630);
#25847=PRODUCT_DEFINITION_FORMATION('',$,#26090);
#25992=APPLICATION_CONTEXT(
'Core Data for Automotive Mechanical Design Process');
#25993=PRODUCT_CONTEXT('part definition',#25992,'mechanical');
#26090=PRODUCT('Plain pivot bush (9)','Plain pivot bush (9)',
'Plain pivot bush (9)',(#25993));
#26171=COLOUR_RGB('Light Blue',0.38,0.62,0.78);
#26172=FILL_AREA_STYLE_COLOUR('',#26171);
#26173=FILL_AREA_STYLE('',(#26172));
#26174=SURFACE_STYLE_FILL_AREA(#26173);
#26175=SURFACE_SIDE_STYLE('',(#26174));
#26176=SURFACE_STYLE_USAGE(.BOTH.,#26175);
#26177=PRESENTATION_STYLE_ASSIGNMENT((#26176));
ENDSEC;
END-ISO-10303-21;
